ISO-10303-21;
HEADER;
/* Generated by software containing ST-Developer
 * from STEP Tools, Inc. (www.steptools.com) 
 */

FILE_DESCRIPTION(
/* description */ ('Rotary union on bearing shaft'),
/* implementation_level */ '2;1');

FILE_NAME(
/* name */ 'Cap Screw - M4x16.step',
/* time_stamp */ '2026-10-28T03:24:01-07:00',
/* author */ (''),
/* organization */ (''),
/* preprocessor_version */ 'ST-DEVELOPER v20.2',
/* originating_system */ 'Autodesk Translation Framework v15.17.0.0',
/* authorisation */ '');

FILE_SCHEMA (('AUTOMOTIVE_DESIGN { 1 0 10303 214 3 1 1 }'));
ENDSEC;

DATA;
#10=MECHANICAL_DESIGN_GEOMETRIC_PRESENTATION_REPRESENTATION('',(#338),#9448);
#12=ORIENTED_CLOSED_SHELL('',*,#4895,.F.);
#15=BREP_WITH_VOIDS('Body1',#4894,(#12));
#209=CONICAL_SURFACE('',#5590,0.325,0.785398163397448);
#210=CONICAL_SURFACE('',#5594,0.335,0.785398163397448);
#211=CONICAL_SURFACE('',#5598,0.21,0.463647609000806);
#212=CONICAL_SURFACE('',#5602,0.18,0.785398163397448);
#276=SHAPE_REPRESENTATION_RELATIONSHIP('SRR','None',#9577,#303);
#303=ADVANCED_BREP_SHAPE_REPRESENTATION('',(#15),#9437);
#338=STYLED_ITEM('',(#9785),#15);
#454=FACE_BOUND('',#1213,.T.);
#578=PLANE('',#5588);
#579=PLANE('',#5596);
#580=PLANE('',#5604);
#581=PLANE('',#5605);
#582=PLANE('',#5606);
#583=PLANE('',#5607);
#584=PLANE('',#5608);
#585=PLANE('',#5609);
#586=PLANE('',#5610);
#587=PLANE('',#5611);
#588=PLANE('',#5612);
#835=FACE_OUTER_BOUND('',#1208,.T.);
#836=FACE_OUTER_BOUND('',#1209,.T.);
#837=FACE_OUTER_BOUND('',#1210,.T.);
#838=FACE_OUTER_BOUND('',#1211,.T.);
#839=FACE_OUTER_BOUND('',#1212,.T.);
#840=FACE_OUTER_BOUND('',#1214,.T.);
#841=FACE_OUTER_BOUND('',#1215,.T.);
#842=FACE_OUTER_BOUND('',#1216,.T.);
#843=FACE_OUTER_BOUND('',#1217,.T.);
#844=FACE_OUTER_BOUND('',#1218,.T.);
#845=FACE_OUTER_BOUND('',#1219,.T.);
#846=FACE_OUTER_BOUND('',#1220,.T.);
#847=FACE_OUTER_BOUND('',#1221,.T.);
#848=FACE_OUTER_BOUND('',#1222,.T.);
#849=FACE_OUTER_BOUND('',#1223,.T.);
#850=FACE_OUTER_BOUND('',#1224,.T.);
#851=FACE_OUTER_BOUND('',#1225,.T.);
#1208=EDGE_LOOP('',(#3999));
#1209=EDGE_LOOP('',(#4000,#4001,#4002,#4003));
#1210=EDGE_LOOP('',(#4004,#4005,#4006,#4007));
#1211=EDGE_LOOP('',(#4008,#4009,#4010,#4011));
#1212=EDGE_LOOP('',(#4012));
#1213=EDGE_LOOP('',(#4013));
#1214=EDGE_LOOP('',(#4014,#4015,#4016,#4017));
#1215=EDGE_LOOP('',(#4018,#4019,#4020,#4021));
#1216=EDGE_LOOP('',(#4022,#4023,#4024,#4025));
#1217=EDGE_LOOP('',(#4026));
#1218=EDGE_LOOP('',(#4027,#4028,#4029,#4030));
#1219=EDGE_LOOP('',(#4031,#4032,#4033,#4034));
#1220=EDGE_LOOP('',(#4035,#4036,#4037,#4038));
#1221=EDGE_LOOP('',(#4039,#4040,#4041,#4042));
#1222=EDGE_LOOP('',(#4043,#4044,#4045,#4046));
#1223=EDGE_LOOP('',(#4047,#4048,#4049,#4050));
#1224=EDGE_LOOP('',(#4051,#4052,#4053,#4054,#4055,#4056));
#1225=EDGE_LOOP('',(#4057,#4058,#4059,#4060,#4061,#4062));
#1522=LINE('',#8691,#1842);
#1523=LINE('',#8695,#1843);
#1524=LINE('',#8699,#1844);
#1525=LINE('',#8706,#1845);
#1526=LINE('',#8710,#1846);
#1527=LINE('',#8714,#1847);
#1528=LINE('',#8719,#1848);
#1529=LINE('',#8721,#1849);
#1530=LINE('',#8723,#1850);
#1531=LINE('',#8724,#1851);
#1532=LINE('',#8727,#1852);
#1533=LINE('',#8729,#1853);
#1534=LINE('',#8730,#1854);
#1535=LINE('',#8733,#1855);
#1536=LINE('',#8735,#1856);
#1537=LINE('',#8736,#1857);
#1538=LINE('',#8739,#1858);
#1539=LINE('',#8741,#1859);
#1540=LINE('',#8742,#1860);
#1541=LINE('',#8745,#1861);
#1542=LINE('',#8747,#1862);
#1543=LINE('',#8748,#1863);
#1544=LINE('',#8750,#1864);
#1545=LINE('',#8751,#1865);
#1842=VECTOR('',#6765,0.325);
#1843=VECTOR('',#6770,0.35);
#1844=VECTOR('',#6775,0.335);
#1845=VECTOR('',#6784,0.21);
#1846=VECTOR('',#6789,0.2);
#1847=VECTOR('',#6794,0.18);
#1848=VECTOR('',#6799,1.);
#1849=VECTOR('',#6800,1.);
#1850=VECTOR('',#6801,1.);
#1851=VECTOR('',#6802,1.);
#1852=VECTOR('',#6805,1.);
#1853=VECTOR('',#6806,1.);
#1854=VECTOR('',#6807,1.);
#1855=VECTOR('',#6810,1.);
#1856=VECTOR('',#6811,1.);
#1857=VECTOR('',#6812,1.);
#1858=VECTOR('',#6815,1.);
#1859=VECTOR('',#6816,1.);
#1860=VECTOR('',#6817,1.);
#1861=VECTOR('',#6820,1.);
#1862=VECTOR('',#6821,1.);
#1863=VECTOR('',#6822,1.);
#1864=VECTOR('',#6825,1.);
#1865=VECTOR('',#6826,1.);
#2180=CIRCLE('',#5589,0.3);
#2181=CIRCLE('',#5591,0.35);
#2182=CIRCLE('',#5593,0.35);
#2183=CIRCLE('',#5595,0.32);
#2184=CIRCLE('',#5597,0.22);
#2185=CIRCLE('',#5599,0.1954);
#2186=CIRCLE('',#5601,0.1954);
#2187=CIRCLE('',#5603,0.16);
#2504=VERTEX_POINT('',#8686);
#2505=VERTEX_POINT('',#8689);
#2506=VERTEX_POINT('',#8693);
#2507=VERTEX_POINT('',#8697);
#2508=VERTEX_POINT('',#8701);
#2509=VERTEX_POINT('',#8704);
#2510=VERTEX_POINT('',#8708);
#2511=VERTEX_POINT('',#8712);
#2512=VERTEX_POINT('',#8717);
#2513=VERTEX_POINT('',#8718);
#2514=VERTEX_POINT('',#8720);
#2515=VERTEX_POINT('',#8722);
#2516=VERTEX_POINT('',#8726);
#2517=VERTEX_POINT('',#8728);
#2518=VERTEX_POINT('',#8732);
#2519=VERTEX_POINT('',#8734);
#2520=VERTEX_POINT('',#8738);
#2521=VERTEX_POINT('',#8740);
#2522=VERTEX_POINT('',#8744);
#2523=VERTEX_POINT('',#8746);
#3027=EDGE_CURVE('',#2504,#2504,#2180,.T.);
#3028=EDGE_CURVE('',#2505,#2505,#2181,.T.);
#3029=EDGE_CURVE('',#2505,#2504,#1522,.T.);
#3030=EDGE_CURVE('',#2506,#2506,#2182,.T.);
#3031=EDGE_CURVE('',#2506,#2505,#1523,.T.);
#3032=EDGE_CURVE('',#2507,#2507,#2183,.T.);
#3033=EDGE_CURVE('',#2507,#2506,#1524,.T.);
#3034=EDGE_CURVE('',#2508,#2508,#2184,.T.);
#3035=EDGE_CURVE('',#2509,#2509,#2185,.F.);
#3036=EDGE_CURVE('',#2509,#2508,#1525,.T.);
#3037=EDGE_CURVE('',#2510,#2510,#2186,.F.);
#3038=EDGE_CURVE('',#2510,#2509,#1526,.T.);
#3039=EDGE_CURVE('',#2511,#2511,#2187,.T.);
#3040=EDGE_CURVE('',#2511,#2510,#1527,.T.);
#3041=EDGE_CURVE('',#2512,#2513,#1528,.T.);
#3042=EDGE_CURVE('',#2513,#2514,#1529,.T.);
#3043=EDGE_CURVE('',#2514,#2515,#1530,.T.);
#3044=EDGE_CURVE('',#2512,#2515,#1531,.T.);
#3045=EDGE_CURVE('',#2513,#2516,#1532,.T.);
#3046=EDGE_CURVE('',#2516,#2517,#1533,.T.);
#3047=EDGE_CURVE('',#2517,#2514,#1534,.T.);
#3048=EDGE_CURVE('',#2516,#2518,#1535,.T.);
#3049=EDGE_CURVE('',#2518,#2519,#1536,.T.);
#3050=EDGE_CURVE('',#2519,#2517,#1537,.T.);
#3051=EDGE_CURVE('',#2518,#2520,#1538,.T.);
#3052=EDGE_CURVE('',#2520,#2521,#1539,.T.);
#3053=EDGE_CURVE('',#2521,#2519,#1540,.T.);
#3054=EDGE_CURVE('',#2520,#2522,#1541,.T.);
#3055=EDGE_CURVE('',#2522,#2523,#1542,.T.);
#3056=EDGE_CURVE('',#2523,#2521,#1543,.T.);
#3057=EDGE_CURVE('',#2522,#2512,#1544,.T.);
#3058=EDGE_CURVE('',#2515,#2523,#1545,.T.);
#3999=ORIENTED_EDGE('',*,*,#3027,.F.);
#4000=ORIENTED_EDGE('',*,*,#3028,.F.);
#4001=ORIENTED_EDGE('',*,*,#3029,.T.);
#4002=ORIENTED_EDGE('',*,*,#3027,.T.);
#4003=ORIENTED_EDGE('',*,*,#3029,.F.);
#4004=ORIENTED_EDGE('',*,*,#3030,.F.);
#4005=ORIENTED_EDGE('',*,*,#3031,.T.);
#4006=ORIENTED_EDGE('',*,*,#3028,.T.);
#4007=ORIENTED_EDGE('',*,*,#3031,.F.);
#4008=ORIENTED_EDGE('',*,*,#3032,.F.);
#4009=ORIENTED_EDGE('',*,*,#3033,.T.);
#4010=ORIENTED_EDGE('',*,*,#3030,.T.);
#4011=ORIENTED_EDGE('',*,*,#3033,.F.);
#4012=ORIENTED_EDGE('',*,*,#3032,.T.);
#4013=ORIENTED_EDGE('',*,*,#3034,.F.);
#4014=ORIENTED_EDGE('',*,*,#3035,.F.);
#4015=ORIENTED_EDGE('',*,*,#3036,.T.);
#4016=ORIENTED_EDGE('',*,*,#3034,.T.);
#4017=ORIENTED_EDGE('',*,*,#3036,.F.);
#4018=ORIENTED_EDGE('',*,*,#3037,.F.);
#4019=ORIENTED_EDGE('',*,*,#3038,.T.);
#4020=ORIENTED_EDGE('',*,*,#3035,.T.);
#4021=ORIENTED_EDGE('',*,*,#3038,.F.);
#4022=ORIENTED_EDGE('',*,*,#3039,.F.);
#4023=ORIENTED_EDGE('',*,*,#3040,.T.);
#4024=ORIENTED_EDGE('',*,*,#3037,.T.);
#4025=ORIENTED_EDGE('',*,*,#3040,.F.);
#4026=ORIENTED_EDGE('',*,*,#3039,.T.);
#4027=ORIENTED_EDGE('',*,*,#3041,.T.);
#4028=ORIENTED_EDGE('',*,*,#3042,.T.);
#4029=ORIENTED_EDGE('',*,*,#3043,.T.);
#4030=ORIENTED_EDGE('',*,*,#3044,.F.);
#4031=ORIENTED_EDGE('',*,*,#3045,.T.);
#4032=ORIENTED_EDGE('',*,*,#3046,.T.);
#4033=ORIENTED_EDGE('',*,*,#3047,.T.);
#4034=ORIENTED_EDGE('',*,*,#3042,.F.);
#4035=ORIENTED_EDGE('',*,*,#3048,.T.);
#4036=ORIENTED_EDGE('',*,*,#3049,.T.);
#4037=ORIENTED_EDGE('',*,*,#3050,.T.);
#4038=ORIENTED_EDGE('',*,*,#3046,.F.);
#4039=ORIENTED_EDGE('',*,*,#3051,.T.);
#4040=ORIENTED_EDGE('',*,*,#3052,.T.);
#4041=ORIENTED_EDGE('',*,*,#3053,.T.);
#4042=ORIENTED_EDGE('',*,*,#3049,.F.);
#4043=ORIENTED_EDGE('',*,*,#3054,.T.);
#4044=ORIENTED_EDGE('',*,*,#3055,.T.);
#4045=ORIENTED_EDGE('',*,*,#3056,.T.);
#4046=ORIENTED_EDGE('',*,*,#3052,.F.);
#4047=ORIENTED_EDGE('',*,*,#3057,.T.);
#4048=ORIENTED_EDGE('',*,*,#3044,.T.);
#4049=ORIENTED_EDGE('',*,*,#3058,.T.);
#4050=ORIENTED_EDGE('',*,*,#3055,.F.);
#4051=ORIENTED_EDGE('',*,*,#3057,.F.);
#4052=ORIENTED_EDGE('',*,*,#3054,.F.);
#4053=ORIENTED_EDGE('',*,*,#3051,.F.);
#4054=ORIENTED_EDGE('',*,*,#3048,.F.);
#4055=ORIENTED_EDGE('',*,*,#3045,.F.);
#4056=ORIENTED_EDGE('',*,*,#3041,.F.);
#4057=ORIENTED_EDGE('',*,*,#3058,.F.);
#4058=ORIENTED_EDGE('',*,*,#3043,.F.);
#4059=ORIENTED_EDGE('',*,*,#3047,.F.);
#4060=ORIENTED_EDGE('',*,*,#3050,.F.);
#4061=ORIENTED_EDGE('',*,*,#3053,.F.);
#4062=ORIENTED_EDGE('',*,*,#3056,.F.);
#4539=CYLINDRICAL_SURFACE('',#5592,0.35);
#4540=CYLINDRICAL_SURFACE('',#5600,0.1954);
#4748=ADVANCED_FACE('',(#835),#578,.T.);
#4749=ADVANCED_FACE('',(#836),#209,.T.);
#4750=ADVANCED_FACE('',(#837),#4539,.T.);
#4751=ADVANCED_FACE('',(#838),#210,.T.);
#4752=ADVANCED_FACE('',(#839,#454),#579,.T.);
#4753=ADVANCED_FACE('',(#840),#211,.T.);
#4754=ADVANCED_FACE('',(#841),#4540,.T.);
#4755=ADVANCED_FACE('',(#842),#212,.T.);
#4756=ADVANCED_FACE('',(#843),#580,.T.);
#4757=ADVANCED_FACE('',(#844),#581,.F.);
#4758=ADVANCED_FACE('',(#845),#582,.F.);
#4759=ADVANCED_FACE('',(#846),#583,.F.);
#4760=ADVANCED_FACE('',(#847),#584,.F.);
#4761=ADVANCED_FACE('',(#848),#585,.F.);
#4762=ADVANCED_FACE('',(#849),#586,.F.);
#4763=ADVANCED_FACE('',(#850),#587,.F.);
#4764=ADVANCED_FACE('',(#851),#588,.F.);
#4894=CLOSED_SHELL('',(#4748,#4749,#4750,#4751,#4752,#4753,#4754,#4755,
#4756));
#4895=CLOSED_SHELL('',(#4757,#4758,#4759,#4760,#4761,#4762,#4763,#4764));
#5587=AXIS2_PLACEMENT_3D('',#8684,#6755,#6756);
#5588=AXIS2_PLACEMENT_3D('',#8685,#6757,#6758);
#5589=AXIS2_PLACEMENT_3D('',#8687,#6759,#6760);
#5590=AXIS2_PLACEMENT_3D('',#8688,#6761,#6762);
#5591=AXIS2_PLACEMENT_3D('',#8690,#6763,#6764);
#5592=AXIS2_PLACEMENT_3D('',#8692,#6766,#6767);
#5593=AXIS2_PLACEMENT_3D('',#8694,#6768,#6769);
#5594=AXIS2_PLACEMENT_3D('',#8696,#6771,#6772);
#5595=AXIS2_PLACEMENT_3D('',#8698,#6773,#6774);
#5596=AXIS2_PLACEMENT_3D('',#8700,#6776,#6777);
#5597=AXIS2_PLACEMENT_3D('',#8702,#6778,#6779);
#5598=AXIS2_PLACEMENT_3D('',#8703,#6780,#6781);
#5599=AXIS2_PLACEMENT_3D('',#8705,#6782,#6783);
#5600=AXIS2_PLACEMENT_3D('',#8707,#6785,#6786);
#5601=AXIS2_PLACEMENT_3D('',#8709,#6787,#6788);
#5602=AXIS2_PLACEMENT_3D('',#8711,#6790,#6791);
#5603=AXIS2_PLACEMENT_3D('',#8713,#6792,#6793);
#5604=AXIS2_PLACEMENT_3D('',#8715,#6795,#6796);
#5605=AXIS2_PLACEMENT_3D('',#8716,#6797,#6798);
#5606=AXIS2_PLACEMENT_3D('',#8725,#6803,#6804);
#5607=AXIS2_PLACEMENT_3D('',#8731,#6808,#6809);
#5608=AXIS2_PLACEMENT_3D('',#8737,#6813,#6814);
#5609=AXIS2_PLACEMENT_3D('',#8743,#6818,#6819);
#5610=AXIS2_PLACEMENT_3D('',#8749,#6823,#6824);
#5611=AXIS2_PLACEMENT_3D('',#8752,#6827,#6828);
#5612=AXIS2_PLACEMENT_3D('',#8753,#6829,#6830);
#6755=DIRECTION('axis',(0.,0.,1.));
#6756=DIRECTION('refdir',(1.,0.,0.));
#6757=DIRECTION('center_axis',(0.,1.,0.));
#6758=DIRECTION('ref_axis',(0.,0.,1.));
#6759=DIRECTION('center_axis',(0.,-1.,0.));
#6760=DIRECTION('ref_axis',(1.,0.,0.));
#6761=DIRECTION('center_axis',(0.,-1.,0.));
#6762=DIRECTION('ref_axis',(1.,0.,0.));
#6763=DIRECTION('center_axis',(0.,-1.,0.));
#6764=DIRECTION('ref_axis',(1.,0.,0.));
#6765=DIRECTION('',(0.707106781186547,0.707106781186548,8.65956056235493E-17));
#6766=DIRECTION('center_axis',(0.,-1.,0.));
#6767=DIRECTION('ref_axis',(1.,0.,0.));
#6768=DIRECTION('center_axis',(0.,-1.,0.));
#6769=DIRECTION('ref_axis',(1.,0.,0.));
#6770=DIRECTION('',(0.,1.,0.));
#6771=DIRECTION('center_axis',(0.,1.,0.));
#6772=DIRECTION('ref_axis',(1.,0.,0.));
#6773=DIRECTION('center_axis',(0.,-1.,0.));
#6774=DIRECTION('ref_axis',(1.,0.,0.));
#6775=DIRECTION('',(-0.707106781186547,0.707106781186548,-8.65956056235493E-17));
#6776=DIRECTION('center_axis',(0.,-1.,0.));
#6777=DIRECTION('ref_axis',(0.,0.,-1.));
#6778=DIRECTION('center_axis',(0.,-1.,0.));
#6779=DIRECTION('ref_axis',(1.,0.,0.));
#6780=DIRECTION('center_axis',(0.,1.,0.));
#6781=DIRECTION('ref_axis',(1.,0.,0.));
#6782=DIRECTION('center_axis',(0.,1.,0.));
#6783=DIRECTION('ref_axis',(1.,0.,0.));
#6784=DIRECTION('',(-0.447213595499958,0.894427190999916,-5.47678698264203E-17));
#6785=DIRECTION('center_axis',(0.,-1.,0.));
#6786=DIRECTION('ref_axis',(1.,0.,0.));
#6787=DIRECTION('center_axis',(0.,1.,0.));
#6788=DIRECTION('ref_axis',(1.,0.,0.));
#6789=DIRECTION('',(0.,1.,0.));
#6790=DIRECTION('center_axis',(0.,1.,0.));
#6791=DIRECTION('ref_axis',(1.,0.,0.));
#6792=DIRECTION('center_axis',(0.,-1.,0.));
#6793=DIRECTION('ref_axis',(1.,0.,0.));
#6794=DIRECTION('',(-0.707106781186547,0.707106781186548,-8.65956056235493E-17));
#6795=DIRECTION('center_axis',(0.,-1.,0.));
#6796=DIRECTION('ref_axis',(0.,0.,-1.));
#6797=DIRECTION('center_axis',(0.866025403784439,0.,-0.5));
#6798=DIRECTION('ref_axis',(0.5,0.,0.866025403784439));
#6799=DIRECTION('',(-0.5,0.,-0.866025403784439));
#6800=DIRECTION('',(0.,-1.,0.));
#6801=DIRECTION('',(0.5,0.,0.866025403784439));
#6802=DIRECTION('',(0.,-1.,0.));
#6803=DIRECTION('center_axis',(1.60246890531964E-16,0.,-1.));
#6804=DIRECTION('ref_axis',(1.,0.,1.60246890531964E-16));
#6805=DIRECTION('',(-1.,0.,-1.60246890531964E-16));
#6806=DIRECTION('',(0.,-1.,0.));
#6807=DIRECTION('',(1.,0.,1.60246890531964E-16));
#6808=DIRECTION('center_axis',(-0.866025403784439,0.,-0.5));
#6809=DIRECTION('ref_axis',(0.5,0.,-0.866025403784439));
#6810=DIRECTION('',(-0.5,0.,0.866025403784439));
#6811=DIRECTION('',(0.,-1.,0.));
#6812=DIRECTION('',(0.5,0.,-0.866025403784439));
#6813=DIRECTION('center_axis',(-0.866025403784439,0.,0.5));
#6814=DIRECTION('ref_axis',(-0.5,0.,-0.866025403784439));
#6815=DIRECTION('',(0.5,0.,0.866025403784439));
#6816=DIRECTION('',(0.,-1.,0.));
#6817=DIRECTION('',(-0.5,0.,-0.866025403784439));
#6818=DIRECTION('center_axis',(-1.60246890531964E-16,0.,1.));
#6819=DIRECTION('ref_axis',(-1.,0.,-1.60246890531964E-16));
#6820=DIRECTION('',(1.,0.,1.60246890531964E-16));
#6821=DIRECTION('',(0.,-1.,0.));
#6822=DIRECTION('',(-1.,0.,-1.60246890531964E-16));
#6823=DIRECTION('center_axis',(0.866025403784439,0.,0.5));
#6824=DIRECTION('ref_axis',(-0.5,0.,0.866025403784439));
#6825=DIRECTION('',(0.5,0.,-0.866025403784439));
#6826=DIRECTION('',(-0.5,0.,0.866025403784439));
#6827=DIRECTION('center_axis',(0.,1.,0.));
#6828=DIRECTION('ref_axis',(1.,0.,0.));
#6829=DIRECTION('center_axis',(0.,-1.,0.));
#6830=DIRECTION('ref_axis',(0.,0.,-1.));
#8684=CARTESIAN_POINT('',(0.,0.,0.));
#8685=CARTESIAN_POINT('Origin',(0.3,0.4,0.));
#8686=CARTESIAN_POINT('',(-0.3,0.4,-3.67394039744206E-17));
#8687=CARTESIAN_POINT('Origin',(0.,0.4,0.));
#8688=CARTESIAN_POINT('Origin',(0.,0.375,0.));
#8689=CARTESIAN_POINT('',(-0.35,0.35,-4.28626379701573E-17));
#8690=CARTESIAN_POINT('Origin',(0.,0.35,0.));
#8691=CARTESIAN_POINT('',(-0.325,0.375,-3.9801020972289E-17));
#8692=CARTESIAN_POINT('Origin',(0.,0.19,0.));
#8693=CARTESIAN_POINT('',(-0.35,0.03,-4.28626379701574E-17));
#8694=CARTESIAN_POINT('Origin',(0.,0.03,0.));
#8695=CARTESIAN_POINT('',(-0.35,0.19,-4.28626379701574E-17));
#8696=CARTESIAN_POINT('Origin',(0.,0.0149999999999999,0.));
#8697=CARTESIAN_POINT('',(-0.32,-3.29597460435593E-17,-3.91886975727153E-17));
#8698=CARTESIAN_POINT('Origin',(0.,0.,0.));
#8699=CARTESIAN_POINT('',(-0.335,0.0149999999999999,-4.10256677714363E-17));
#8700=CARTESIAN_POINT('Origin',(0.22,0.,0.));
#8701=CARTESIAN_POINT('',(-0.22,-6.93889390390723E-18,-2.69422295812418E-17));
#8702=CARTESIAN_POINT('Origin',(0.,0.,0.));
#8703=CARTESIAN_POINT('Origin',(0.,-0.02,0.));
#8704=CARTESIAN_POINT('',(-0.1954,-0.0492,2.39295984553393E-17));
#8705=CARTESIAN_POINT('Origin',(0.,-0.0492,0.));
#8706=CARTESIAN_POINT('',(-0.21,-0.02,-2.57175827820944E-17));
#8707=CARTESIAN_POINT('Origin',(0.,-0.8,0.));
#8708=CARTESIAN_POINT('',(-0.1954,-1.5646,2.39295984553393E-17));
#8709=CARTESIAN_POINT('Origin',(0.,-1.5646,0.));
#8710=CARTESIAN_POINT('',(-0.1954,-0.8,-2.39295984553393E-17));
#8711=CARTESIAN_POINT('Origin',(0.,-1.58,0.));
#8712=CARTESIAN_POINT('',(-0.16,-1.6,-1.95943487863577E-17));
#8713=CARTESIAN_POINT('Origin',(0.,-1.6,0.));
#8714=CARTESIAN_POINT('',(-0.18,-1.58,-2.20436423846524E-17));
#8715=CARTESIAN_POINT('Origin',(0.,-1.6,0.));
#8716=CARTESIAN_POINT('Origin',(0.0866025403784439,-0.4,-0.15));
#8717=CARTESIAN_POINT('',(0.173205080756888,-0.4,0.));
#8718=CARTESIAN_POINT('',(0.0866025403784439,-0.4,-0.15));
#8719=CARTESIAN_POINT('',(0.173205080756888,-0.4,0.));
#8720=CARTESIAN_POINT('',(0.0866025403784439,-0.64,-0.15));
#8721=CARTESIAN_POINT('',(0.0866025403784439,-0.4,-0.15));
#8722=CARTESIAN_POINT('',(0.173205080756888,-0.64,0.));
#8723=CARTESIAN_POINT('',(0.173205080756888,-0.64,0.));
#8724=CARTESIAN_POINT('',(0.173205080756888,-0.4,0.));
#8725=CARTESIAN_POINT('Origin',(-0.0866025403784438,-0.4,-0.15));
#8726=CARTESIAN_POINT('',(-0.0866025403784438,-0.4,-0.15));
#8727=CARTESIAN_POINT('',(0.0866025403784439,-0.4,-0.15));
#8728=CARTESIAN_POINT('',(-0.0866025403784438,-0.64,-0.15));
#8729=CARTESIAN_POINT('',(-0.0866025403784438,-0.4,-0.15));
#8730=CARTESIAN_POINT('',(0.0866025403784439,-0.64,-0.15));
#8731=CARTESIAN_POINT('Origin',(-0.173205080756888,-0.4,-2.77555756156289E-17));
#8732=CARTESIAN_POINT('',(-0.173205080756888,-0.4,-2.12115047744981E-17));
#8733=CARTESIAN_POINT('',(-0.0866025403784438,-0.4,-0.15));
#8734=CARTESIAN_POINT('',(-0.173205080756888,-0.64,-2.77555756156289E-17));
#8735=CARTESIAN_POINT('',(-0.173205080756888,-0.4,-2.12115047744981E-17));
#8736=CARTESIAN_POINT('',(-0.0866025403784438,-0.64,-0.15));
#8737=CARTESIAN_POINT('Origin',(-0.0866025403784439,-0.4,0.15));
#8738=CARTESIAN_POINT('',(-0.0866025403784439,-0.4,0.15));
#8739=CARTESIAN_POINT('',(-0.173205080756888,-0.4,-2.12115047744981E-17));
#8740=CARTESIAN_POINT('',(-0.0866025403784439,-0.64,0.15));
#8741=CARTESIAN_POINT('',(-0.0866025403784439,-0.4,0.15));
#8742=CARTESIAN_POINT('',(-0.173205080756888,-0.64,-2.12115047744981E-17));
#8743=CARTESIAN_POINT('Origin',(0.0866025403784439,-0.4,0.15));
#8744=CARTESIAN_POINT('',(0.0866025403784439,-0.4,0.15));
#8745=CARTESIAN_POINT('',(-0.0866025403784439,-0.4,0.15));
#8746=CARTESIAN_POINT('',(0.0866025403784439,-0.64,0.15));
#8747=CARTESIAN_POINT('',(0.0866025403784439,-0.4,0.15));
#8748=CARTESIAN_POINT('',(-0.0866025403784439,-0.64,0.15));
#8749=CARTESIAN_POINT('Origin',(0.173205080756888,-0.4,0.));
#8750=CARTESIAN_POINT('',(0.0866025403784439,-0.4,0.15));
#8751=CARTESIAN_POINT('',(0.0866025403784439,-0.64,0.15));
#8752=CARTESIAN_POINT('Origin',(0.,-0.4,-2.77555756156289E-17));
#8753=CARTESIAN_POINT('Origin',(0.,-0.64,-2.77555756156289E-17));
#9405=UNCERTAINTY_MEASURE_WITH_UNIT(LENGTH_MEASURE(0.001),#9449,
'DISTANCE_ACCURACY_VALUE',
'Maximum model space distance between geometric entities at asserted c
onnectivities');
#9416=UNCERTAINTY_MEASURE_WITH_UNIT(LENGTH_MEASURE(0.001),#9449,
'DISTANCE_ACCURACY_VALUE',
'Maximum model space distance between geometric entities at asserted c
onnectivities');
#9437=(
GEOMETRIC_REPRESENTATION_CONTEXT(3)
GLOBAL_UNCERTAINTY_ASSIGNED_CONTEXT((#9405))
GLOBAL_UNIT_ASSIGNED_CONTEXT((#9449,#9451,#9452))
REPRESENTATION_CONTEXT('','3D')
);
#9448=(
GEOMETRIC_REPRESENTATION_CONTEXT(3)
GLOBAL_UNCERTAINTY_ASSIGNED_CONTEXT((#9416))
GLOBAL_UNIT_ASSIGNED_CONTEXT((#9449,#9451,#9452))
REPRESENTATION_CONTEXT('','3D')
);
#9449=(
LENGTH_UNIT()
NAMED_UNIT(*)
SI_UNIT(.CENTI.,.METRE.)
);
#9451=(
NAMED_UNIT(*)
PLANE_ANGLE_UNIT()
SI_UNIT($,.RADIAN.)
);
#9452=(
NAMED_UNIT(*)
SI_UNIT($,.STERADIAN.)
SOLID_ANGLE_UNIT()
);
#9473=SHAPE_DEFINITION_REPRESENTATION(#9509,#9577);
#9509=PRODUCT_DEFINITION_SHAPE('',$,#9609);
#9577=SHAPE_REPRESENTATION('',(#5587),#9437);
#9588=PRODUCT_DEFINITION_CONTEXT('part definition',#9683,'design');
#9609=PRODUCT_DEFINITION('Cap Screw - M4x16','Cap Screw - M4x16',#9640,
#9588);
#9640=PRODUCT_DEFINITION_FORMATION('',$,#9705);
#9683=APPLICATION_CONTEXT(
'Core Data for Automotive Mechanical Design Process');
#9684=PRODUCT_CONTEXT('part definition',#9683,'mechanical');
#9705=PRODUCT('Cap Screw - M4x16','Cap Screw - M4x16',
'Cap Screw - M4x16',(#9684));
#9779=COLOUR_RGB('Black',0.12,0.14,0.17);
#9780=FILL_AREA_STYLE_COLOUR('',#9779);
#9781=FILL_AREA_STYLE('',(#9780));
#9782=SURFACE_STYLE_FILL_AREA(#9781);
#9783=SURFACE_SIDE_STYLE('',(#9782));
#9784=SURFACE_STYLE_USAGE(.BOTH.,#9783);
#9785=PRESENTATION_STYLE_ASSIGNMENT((#9784));
ENDSEC;
END-ISO-10303-21;
